ISO-10303-21;
HEADER;
/* Generated by software containing ST-Developer
 * from STEP Tools, Inc. (www.steptools.com) 
 */

FILE_DESCRIPTION(
/* description */ (''),
/* implementation_level */ '2;1');

FILE_NAME(
/* name */ 'Rod_Mount_01.step',
/* time_stamp */ '2026-10-19T02:00:06+06:00',
/* author */ (''),
/* organization */ (''),
/* preprocessor_version */ 'ST-DEVELOPER v20.2',
/* originating_system */ 'Autodesk Translation Framework v15.15.0.0',
/* authorisation */ '');

FILE_SCHEMA (('AUTOMOTIVE_DESIGN { 1 0 10303 214 3 1 1 }'));
ENDSEC;

DATA;
#10=MECHANICAL_DESIGN_GEOMETRIC_PRESENTATION_REPRESENTATION('',(#110),#4833);
#88=SHAPE_REPRESENTATION_RELATIONSHIP('SRR','None',#4879,#99);
#99=ADVANCED_BREP_SHAPE_REPRESENTATION('',(#121),#4827);
#110=STYLED_ITEM('',(#4992),#121);
#121=MANIFOLD_SOLID_BREP('Rod_Mount_01',#2692);
#139=FACE_BOUND('',#521,.T.);
#140=FACE_BOUND('',#524,.T.);
#141=FACE_BOUND('',#526,.T.);
#212=PLANE('',#2952);
#213=PLANE('',#2956);
#214=PLANE('',#2957);
#345=FACE_OUTER_BOUND('',#518,.T.);
#346=FACE_OUTER_BOUND('',#519,.T.);
#347=FACE_OUTER_BOUND('',#520,.T.);
#348=FACE_OUTER_BOUND('',#522,.T.);
#349=FACE_OUTER_BOUND('',#523,.T.);
#350=FACE_OUTER_BOUND('',#525,.T.);
#518=EDGE_LOOP('',(#2075,#2076,#2077,#2078));
#519=EDGE_LOOP('',(#2079,#2080,#2081,#2082));
#520=EDGE_LOOP('',(#2083));
#521=EDGE_LOOP('',(#2084));
#522=EDGE_LOOP('',(#2085,#2086,#2087,#2088));
#523=EDGE_LOOP('',(#2089));
#524=EDGE_LOOP('',(#2090));
#525=EDGE_LOOP('',(#2091));
#526=EDGE_LOOP('',(#2092));
#734=LINE('',#4215,#988);
#735=LINE('',#4221,#989);
#736=LINE('',#4228,#990);
#988=VECTOR('',#3453,7.);
#989=VECTOR('',#3460,6.);
#990=VECTOR('',#3469,11.);
#1161=CIRCLE('',#2947,7.);
#1162=CIRCLE('',#2948,7.);
#1163=CIRCLE('',#2950,6.);
#1164=CIRCLE('',#2951,6.);
#1165=CIRCLE('',#2954,11.);
#1166=CIRCLE('',#2955,11.);
#1299=VERTEX_POINT('',#4212);
#1300=VERTEX_POINT('',#4214);
#1301=VERTEX_POINT('',#4218);
#1302=VERTEX_POINT('',#4220);
#1303=VERTEX_POINT('',#4225);
#1304=VERTEX_POINT('',#4227);
#1578=EDGE_CURVE('',#1299,#1299,#1161,.T.);
#1579=EDGE_CURVE('',#1299,#1300,#734,.T.);
#1580=EDGE_CURVE('',#1300,#1300,#1162,.T.);
#1581=EDGE_CURVE('',#1301,#1301,#1163,.T.);
#1582=EDGE_CURVE('',#1301,#1302,#735,.T.);
#1583=EDGE_CURVE('',#1302,#1302,#1164,.T.);
#1584=EDGE_CURVE('',#1303,#1303,#1165,.T.);
#1585=EDGE_CURVE('',#1303,#1304,#736,.T.);
#1586=EDGE_CURVE('',#1304,#1304,#1166,.T.);
#2075=ORIENTED_EDGE('',*,*,#1578,.F.);
#2076=ORIENTED_EDGE('',*,*,#1579,.T.);
#2077=ORIENTED_EDGE('',*,*,#1580,.F.);
#2078=ORIENTED_EDGE('',*,*,#1579,.F.);
#2079=ORIENTED_EDGE('',*,*,#1581,.F.);
#2080=ORIENTED_EDGE('',*,*,#1582,.T.);
#2081=ORIENTED_EDGE('',*,*,#1583,.T.);
#2082=ORIENTED_EDGE('',*,*,#1582,.F.);
#2083=ORIENTED_EDGE('',*,*,#1578,.T.);
#2084=ORIENTED_EDGE('',*,*,#1581,.T.);
#2085=ORIENTED_EDGE('',*,*,#1584,.F.);
#2086=ORIENTED_EDGE('',*,*,#1585,.T.);
#2087=ORIENTED_EDGE('',*,*,#1586,.T.);
#2088=ORIENTED_EDGE('',*,*,#1585,.F.);
#2089=ORIENTED_EDGE('',*,*,#1584,.T.);
#2090=ORIENTED_EDGE('',*,*,#1580,.T.);
#2091=ORIENTED_EDGE('',*,*,#1586,.F.);
#2092=ORIENTED_EDGE('',*,*,#1583,.F.);
#2502=CYLINDRICAL_SURFACE('',#2946,7.);
#2503=CYLINDRICAL_SURFACE('',#2949,6.);
#2504=CYLINDRICAL_SURFACE('',#2953,11.);
#2603=ADVANCED_FACE('',(#345),#2502,.T.);
#2604=ADVANCED_FACE('',(#346),#2503,.F.);
#2605=ADVANCED_FACE('',(#347,#139),#212,.T.);
#2606=ADVANCED_FACE('',(#348),#2504,.T.);
#2607=ADVANCED_FACE('',(#349,#140),#213,.T.);
#2608=ADVANCED_FACE('',(#350,#141),#214,.F.);
#2692=CLOSED_SHELL('',(#2603,#2604,#2605,#2606,#2607,#2608));
#2945=AXIS2_PLACEMENT_3D('',#4210,#3447,#3448);
#2946=AXIS2_PLACEMENT_3D('',#4211,#3449,#3450);
#2947=AXIS2_PLACEMENT_3D('',#4213,#3451,#3452);
#2948=AXIS2_PLACEMENT_3D('',#4216,#3454,#3455);
#2949=AXIS2_PLACEMENT_3D('',#4217,#3456,#3457);
#2950=AXIS2_PLACEMENT_3D('',#4219,#3458,#3459);
#2951=AXIS2_PLACEMENT_3D('',#4222,#3461,#3462);
#2952=AXIS2_PLACEMENT_3D('',#4223,#3463,#3464);
#2953=AXIS2_PLACEMENT_3D('',#4224,#3465,#3466);
#2954=AXIS2_PLACEMENT_3D('',#4226,#3467,#3468);
#2955=AXIS2_PLACEMENT_3D('',#4229,#3470,#3471);
#2956=AXIS2_PLACEMENT_3D('',#4230,#3472,#3473);
#2957=AXIS2_PLACEMENT_3D('',#4231,#3474,#3475);
#3447=DIRECTION('axis',(0.,0.,1.));
#3448=DIRECTION('refdir',(1.,0.,0.));
#3449=DIRECTION('center_axis',(-1.,0.,0.));
#3450=DIRECTION('ref_axis',(0.,-1.,0.));
#3451=DIRECTION('center_axis',(-1.,0.,0.));
#3452=DIRECTION('ref_axis',(0.,-1.,0.));
#3453=DIRECTION('',(1.,0.,0.));
#3454=DIRECTION('center_axis',(1.,0.,0.));
#3455=DIRECTION('ref_axis',(0.,-1.,0.));
#3456=DIRECTION('center_axis',(-1.,0.,0.));
#3457=DIRECTION('ref_axis',(0.,-1.,0.));
#3458=DIRECTION('center_axis',(1.,0.,0.));
#3459=DIRECTION('ref_axis',(0.,-1.,0.));
#3460=DIRECTION('',(1.,0.,0.));
#3461=DIRECTION('center_axis',(1.,0.,0.));
#3462=DIRECTION('ref_axis',(0.,-1.,0.));
#3463=DIRECTION('center_axis',(-1.,0.,0.));
#3464=DIRECTION('ref_axis',(0.,-1.,0.));
#3465=DIRECTION('center_axis',(-1.,0.,0.));
#3466=DIRECTION('ref_axis',(0.,-1.,0.));
#3467=DIRECTION('center_axis',(-1.,0.,0.));
#3468=DIRECTION('ref_axis',(0.,-1.,0.));
#3469=DIRECTION('',(1.,0.,0.));
#3470=DIRECTION('center_axis',(-1.,0.,0.));
#3471=DIRECTION('ref_axis',(0.,-1.,0.));
#3472=DIRECTION('center_axis',(-1.,0.,0.));
#3473=DIRECTION('ref_axis',(0.,-1.,0.));
#3474=DIRECTION('center_axis',(-1.,0.,0.));
#3475=DIRECTION('ref_axis',(0.,-1.,0.));
#4210=CARTESIAN_POINT('',(0.,0.,0.));
#4211=CARTESIAN_POINT('Origin',(70.,-30.0000000000105,7.00000000000211));
#4212=CARTESIAN_POINT('',(60.,-23.0000000000105,7.00000000000211));
#4213=CARTESIAN_POINT('Origin',(60.,-30.0000000000105,7.00000000000211));
#4214=CARTESIAN_POINT('',(69.,-23.0000000000105,7.00000000000211));
#4215=CARTESIAN_POINT('',(70.,-23.0000000000105,7.00000000000211));
#4216=CARTESIAN_POINT('Origin',(69.,-30.0000000000105,7.00000000000211));
#4217=CARTESIAN_POINT('Origin',(70.,-30.0000000000105,7.00000000000211));
#4218=CARTESIAN_POINT('',(60.,-24.0000000000105,7.00000000000211));
#4219=CARTESIAN_POINT('Origin',(60.,-30.0000000000105,7.00000000000211));
#4220=CARTESIAN_POINT('',(70.,-24.0000000000105,7.00000000000211));
#4221=CARTESIAN_POINT('',(70.,-24.0000000000105,7.00000000000211));
#4222=CARTESIAN_POINT('Origin',(70.,-30.0000000000105,7.00000000000211));
#4223=CARTESIAN_POINT('Origin',(60.,-30.0000000000105,7.00000000000211));
#4224=CARTESIAN_POINT('Origin',(70.,-30.0000000000105,7.00000000000211));
#4225=CARTESIAN_POINT('',(69.,-19.0000000000105,7.00000000000211));
#4226=CARTESIAN_POINT('Origin',(69.,-30.0000000000105,7.00000000000211));
#4227=CARTESIAN_POINT('',(70.,-19.0000000000105,7.00000000000211));
#4228=CARTESIAN_POINT('',(70.,-19.0000000000105,7.00000000000211));
#4229=CARTESIAN_POINT('Origin',(70.,-30.0000000000105,7.00000000000211));
#4230=CARTESIAN_POINT('Origin',(69.,-30.0000000000105,7.00000000000211));
#4231=CARTESIAN_POINT('Origin',(70.,-30.0000000000105,7.00000000000211));
#4814=UNCERTAINTY_MEASURE_WITH_UNIT(LENGTH_MEASURE(0.01),#4834,
'DISTANCE_ACCURACY_VALUE',
'Maximum model space distance between geometric entities at asserted c
onnectivities');
#4820=UNCERTAINTY_MEASURE_WITH_UNIT(LENGTH_MEASURE(0.01),#4834,
'DISTANCE_ACCURACY_VALUE',
'Maximum model space distance between geometric entities at asserted c
onnectivities');
#4827=(
GEOMETRIC_REPRESENTATION_CONTEXT(3)
GLOBAL_UNCERTAINTY_ASSIGNED_CONTEXT((#4814))
GLOBAL_UNIT_ASSIGNED_CONTEXT((#4834,#4836,#4837))
REPRESENTATION_CONTEXT('','3D')
);
#4833=(
GEOMETRIC_REPRESENTATION_CONTEXT(3)
GLOBAL_UNCERTAINTY_ASSIGNED_CONTEXT((#4820))
GLOBAL_UNIT_ASSIGNED_CONTEXT((#4834,#4836,#4837))
REPRESENTATION_CONTEXT('','3D')
);
#4834=(
LENGTH_UNIT()
NAMED_UNIT(*)
SI_UNIT(.MILLI.,.METRE.)
);
#4836=(
NAMED_UNIT(*)
PLANE_ANGLE_UNIT()
SI_UNIT($,.RADIAN.)
);
#4837=(
NAMED_UNIT(*)
SI_UNIT($,.STERADIAN.)
SOLID_ANGLE_UNIT()
);
#4844=SHAPE_DEFINITION_REPRESENTATION(#4856,#4879);
#4856=PRODUCT_DEFINITION_SHAPE('',$,#4892);
#4879=SHAPE_REPRESENTATION('',(#2945),#4827);
#4885=PRODUCT_DEFINITION_CONTEXT('part definition',#4923,'design');
#4892=PRODUCT_DEFINITION('Rod_Mount_01','Rod_Mount_01',#4904,#4885);
#4904=PRODUCT_DEFINITION_FORMATION('',$,#4931);
#4923=APPLICATION_CONTEXT(
'Core Data for Automotive Mechanical Design Process');
#4924=PRODUCT_CONTEXT('part definition',#4923,'mechanical');
#4931=PRODUCT('Rod_Mount_01','Rod_Mount_01',$,(#4924));
#4986=COLOUR_RGB('Grey',0.48,0.52,0.57);
#4987=FILL_AREA_STYLE_COLOUR('',#4986);
#4988=FILL_AREA_STYLE('',(#4987));
#4989=SURFACE_STYLE_FILL_AREA(#4988);
#4990=SURFACE_SIDE_STYLE('',(#4989));
#4991=SURFACE_STYLE_USAGE(.BOTH.,#4990);
#4992=PRESENTATION_STYLE_ASSIGNMENT((#4991));
ENDSEC;
END-ISO-10303-21;
